ISO-10303-21;
HEADER;
/* Generated by software containing ST-Developer
 * from STEP Tools, Inc. (www.steptools.com) 
 */

FILE_DESCRIPTION(
/* description */ ('STEP AP214'),
/* implementation_level */ '2;1');

FILE_NAME(
/* name */ 'Screw.step',
/* time_stamp */ '2026-11-14T21:46:24-08:00',
/* author */ (''),
/* organization */ (''),
/* preprocessor_version */ 'ST-DEVELOPER v20.2',
/* originating_system */ 'Autodesk Translation Framework v15.17.0.0',
/* authorisation */ '');

FILE_SCHEMA (('AUTOMOTIVE_DESIGN { 1 0 10303 214 3 1 1 }'));
ENDSEC;

DATA;
#10=MECHANICAL_DESIGN_GEOMETRIC_PRESENTATION_REPRESENTATION('',(#90),#7783);
#76=SHAPE_REPRESENTATION_RELATIONSHIP('SRR','None',#7821,#83);
#83=ADVANCED_BREP_SHAPE_REPRESENTATION('',(#97),#7777);
#90=STYLED_ITEM('',(#7869),#97);
#97=MANIFOLD_SOLID_BREP('Body1',#4165);
#119=FACE_BOUND('',#1393,.T.);
#120=FACE_BOUND('',#1395,.T.);
#121=FACE_BOUND('',#1404,.T.);
#122=FACE_BOUND('',#1419,.T.);
#194=PLANE('',#4357);
#195=PLANE('',#4358);
#196=PLANE('',#4359);
#197=PLANE('',#4360);
#198=PLANE('',#4361);
#199=PLANE('',#4362);
#200=PLANE('',#4363);
#201=PLANE('',#4364);
#202=PLANE('',#4365);
#203=PLANE('',#4366);
#204=PLANE('',#4367);
#205=PLANE('',#4368);
#206=PLANE('',#4369);
#207=PLANE('',#4370);
#208=PLANE('',#4371);
#209=PLANE('',#4372);
#210=PLANE('',#4373);
#211=PLANE('',#4374);
#212=PLANE('',#4375);
#213=PLANE('',#4376);
#214=PLANE('',#4377);
#215=PLANE('',#4378);
#216=PLANE('',#4379);
#217=PLANE('',#4380);
#393=LINE('',#6285,#752);
#394=LINE('',#6291,#753);
#395=LINE('',#6297,#754);
#396=LINE('',#6315,#755);
#397=LINE('',#6320,#756);
#398=LINE('',#6322,#757);
#399=LINE('',#6324,#758);
#400=LINE('',#6326,#759);
#401=LINE('',#6328,#760);
#402=LINE('',#6329,#761);
#403=LINE('',#6333,#762);
#404=LINE('',#6335,#763);
#405=LINE('',#6336,#764);
#406=LINE('',#6339,#765);
#407=LINE('',#6340,#766);
#408=LINE('',#6343,#767);
#409=LINE('',#6344,#768);
#410=LINE('',#6347,#769);
#411=LINE('',#6348,#770);
#412=LINE('',#6351,#771);
#413=LINE('',#6352,#772);
#414=LINE('',#6354,#773);
#415=LINE('',#6359,#774);
#416=LINE('',#6361,#775);
#417=LINE('',#6363,#776);
#418=LINE('',#6365,#777);
#419=LINE('',#6367,#778);
#420=LINE('',#6368,#779);
#421=LINE('',#6371,#780);
#422=LINE('',#6372,#781);
#423=LINE('',#6375,#782);
#424=LINE('',#6376,#783);
#425=LINE('',#6379,#784);
#426=LINE('',#6380,#785);
#427=LINE('',#6383,#786);
#428=LINE('',#6384,#787);
#429=LINE('',#6387,#788);
#430=LINE('',#6388,#789);
#431=LINE('',#6391,#790);
#432=LINE('',#6392,#791);
#433=LINE('',#6394,#792);
#434=LINE('',#6395,#793);
#435=LINE('',#6397,#794);
#436=LINE('',#6399,#795);
#437=LINE('',#6401,#796);
#438=LINE('',#6403,#797);
#752=VECTOR('',#5000,6.);
#753=VECTOR('',#5007,5.);
#754=VECTOR('',#5014,10.);
#755=VECTOR('',#5033,14.);
#756=VECTOR('',#5038,1000.);
#757=VECTOR('',#5039,1000.);
#758=VECTOR('',#5040,1000.);
#759=VECTOR('',#5041,1000.);
#760=VECTOR('',#5042,1000.);
#761=VECTOR('',#5043,1000.);
#762=VECTOR('',#5048,1000.);
#763=VECTOR('',#5049,1000.);
#764=VECTOR('',#5050,1000.);
#765=VECTOR('',#5053,1000.);
#766=VECTOR('',#5054,1000.);
#767=VECTOR('',#5057,1000.);
#768=VECTOR('',#5058,1000.);
#769=VECTOR('',#5061,1000.);
#770=VECTOR('',#5062,1000.);
#771=VECTOR('',#5065,1000.);
#772=VECTOR('',#5066,1000.);
#773=VECTOR('',#5069,1000.);
#774=VECTOR('',#5074,1000.);
#775=VECTOR('',#5075,1000.);
#776=VECTOR('',#5076,1000.);
#777=VECTOR('',#5077,1000.);
#778=VECTOR('',#5078,1000.);
#779=VECTOR('',#5079,1000.);
#780=VECTOR('',#5082,1000.);
#781=VECTOR('',#5083,1000.);
#782=VECTOR('',#5086,1000.);
#783=VECTOR('',#5087,1000.);
#784=VECTOR('',#5090,1000.);
#785=VECTOR('',#5091,1000.);
#786=VECTOR('',#5094,1000.);
#787=VECTOR('',#5095,1000.);
#788=VECTOR('',#5098,1000.);
#789=VECTOR('',#5099,1000.);
#790=VECTOR('',#5102,1000.);
#791=VECTOR('',#5103,1000.);
#792=VECTOR('',#5106,1000.);
#793=VECTOR('',#5107,1000.);
#794=VECTOR('',#5110,1000.);
#795=VECTOR('',#5113,1000.);
#796=VECTOR('',#5116,1000.);
#797=VECTOR('',#5119,1000.);
#1020=CYLINDRICAL_SURFACE('',#4339,6.);
#1021=CYLINDRICAL_SURFACE('',#4342,5.);
#1022=CYLINDRICAL_SURFACE('',#4345,10.);
#1023=CYLINDRICAL_SURFACE('',#4354,14.);
#1138=FACE_OUTER_BOUND('',#1388,.T.);
#1139=FACE_OUTER_BOUND('',#1389,.T.);
#1140=FACE_OUTER_BOUND('',#1390,.T.);
#1141=FACE_OUTER_BOUND('',#1391,.T.);
#1142=FACE_OUTER_BOUND('',#1392,.T.);
#1143=FACE_OUTER_BOUND('',#1394,.T.);
#1144=FACE_OUTER_BOUND('',#1396,.T.);
#1145=FACE_OUTER_BOUND('',#1397,.T.);
#1146=FACE_OUTER_BOUND('',#1398,.T.);
#1147=FACE_OUTER_BOUND('',#1399,.T.);
#1148=FACE_OUTER_BOUND('',#1400,.T.);
#1149=FACE_OUTER_BOUND('',#1401,.T.);
#1150=FACE_OUTER_BOUND('',#1402,.T.);
#1151=FACE_OUTER_BOUND('',#1403,.T.);
#1152=FACE_OUTER_BOUND('',#1405,.T.);
#1153=FACE_OUTER_BOUND('',#1406,.T.);
#1154=FACE_OUTER_BOUND('',#1407,.T.);
#1155=FACE_OUTER_BOUND('',#1408,.T.);
#1156=FACE_OUTER_BOUND('',#1409,.T.);
#1157=FACE_OUTER_BOUND('',#1410,.T.);
#1158=FACE_OUTER_BOUND('',#1411,.T.);
#1159=FACE_OUTER_BOUND('',#1412,.T.);
#1160=FACE_OUTER_BOUND('',#1413,.T.);
#1161=FACE_OUTER_BOUND('',#1414,.T.);
#1162=FACE_OUTER_BOUND('',#1415,.T.);
#1163=FACE_OUTER_BOUND('',#1416,.T.);
#1164=FACE_OUTER_BOUND('',#1417,.T.);
#1165=FACE_OUTER_BOUND('',#1418,.T.);
#1388=EDGE_LOOP('',(#3032,#3033,#3034,#3035));
#1389=EDGE_LOOP('',(#3036,#3037,#3038,#3039));
#1390=EDGE_LOOP('',(#3040,#3041,#3042,#3043,#3044,#3045,#3046,#3047,#3048,
#3049));
#1391=EDGE_LOOP('',(#3050,#3051,#3052,#3053));
#1392=EDGE_LOOP('',(#3054));
#1393=EDGE_LOOP('',(#3055,#3056,#3057,#3058,#3059,#3060));
#1394=EDGE_LOOP('',(#3061));
#1395=EDGE_LOOP('',(#3062));
#1396=EDGE_LOOP('',(#3063,#3064,#3065,#3066));
#1397=EDGE_LOOP('',(#3067,#3068,#3069,#3070));
#1398=EDGE_LOOP('',(#3071,#3072,#3073,#3074));
#1399=EDGE_LOOP('',(#3075,#3076,#3077,#3078));
#1400=EDGE_LOOP('',(#3079,#3080,#3081,#3082));
#1401=EDGE_LOOP('',(#3083,#3084,#3085,#3086));
#1402=EDGE_LOOP('',(#3087,#3088,#3089,#3090,#3091,#3092));
#1403=EDGE_LOOP('',(#3093,#3094,#3095,#3096,#3097,#3098));
#1404=EDGE_LOOP('',(#3099));
#1405=EDGE_LOOP('',(#3100,#3101,#3102));
#1406=EDGE_LOOP('',(#3103,#3104,#3105));
#1407=EDGE_LOOP('',(#3106,#3107,#3108));
#1408=EDGE_LOOP('',(#3109,#3110,#3111));
#1409=EDGE_LOOP('',(#3112,#3113,#3114));
#1410=EDGE_LOOP('',(#3115,#3116,#3117,#3118));
#1411=EDGE_LOOP('',(#3119,#3120,#3121,#3122,#3123));
#1412=EDGE_LOOP('',(#3124,#3125,#3126,#3127,#3128));
#1413=EDGE_LOOP('',(#3129,#3130,#3131,#3132,#3133));
#1414=EDGE_LOOP('',(#3134,#3135,#3136,#3137,#3138));
#1415=EDGE_LOOP('',(#3139,#3140,#3141,#3142,#3143));
#1416=EDGE_LOOP('',(#3144,#3145,#3146,#3147,#3148));
#1417=EDGE_LOOP('',(#3149));
#1418=EDGE_LOOP('',(#3150));
#1419=EDGE_LOOP('',(#3151));
#1652=CIRCLE('',#4340,6.);
#1653=CIRCLE('',#4341,6.);
#1654=CIRCLE('',#4343,5.);
#1655=CIRCLE('',#4344,5.);
#1656=CIRCLE('',#4346,10.);
#1657=CIRCLE('',#4347,10.);
#1658=CIRCLE('',#4348,10.);
#1659=CIRCLE('',#4349,10.);
#1660=CIRCLE('',#4350,10.);
#1661=CIRCLE('',#4351,10.);
#1662=CIRCLE('',#4352,10.);
#1663=CIRCLE('',#4353,10.);
#1664=CIRCLE('',#4355,14.);
#1665=CIRCLE('',#4356,14.);
#1912=VERTEX_POINT('',#6282);
#1913=VERTEX_POINT('',#6284);
#1914=VERTEX_POINT('',#6288);
#1915=VERTEX_POINT('',#6290);
#1916=VERTEX_POINT('',#6294);
#1917=VERTEX_POINT('',#6296);
#1918=VERTEX_POINT('',#6298);
#1919=VERTEX_POINT('',#6300);
#1920=VERTEX_POINT('',#6302);
#1921=VERTEX_POINT('',#6304);
#1922=VERTEX_POINT('',#6306);
#1923=VERTEX_POINT('',#6308);
#1924=VERTEX_POINT('',#6312);
#1925=VERTEX_POINT('',#6314);
#1926=VERTEX_POINT('',#6318);
#1927=VERTEX_POINT('',#6319);
#1928=VERTEX_POINT('',#6321);
#1929=VERTEX_POINT('',#6323);
#1930=VERTEX_POINT('',#6325);
#1931=VERTEX_POINT('',#6327);
#1932=VERTEX_POINT('',#6332);
#1933=VERTEX_POINT('',#6334);
#1934=VERTEX_POINT('',#6338);
#1935=VERTEX_POINT('',#6342);
#1936=VERTEX_POINT('',#6346);
#1937=VERTEX_POINT('',#6350);
#1938=VERTEX_POINT('',#6357);
#1939=VERTEX_POINT('',#6358);
#1940=VERTEX_POINT('',#6360);
#1941=VERTEX_POINT('',#6362);
#1942=VERTEX_POINT('',#6364);
#1943=VERTEX_POINT('',#6366);
#1944=VERTEX_POINT('',#6370);
#1945=VERTEX_POINT('',#6374);
#1946=VERTEX_POINT('',#6378);
#1947=VERTEX_POINT('',#6382);
#1948=VERTEX_POINT('',#6386);
#1949=VERTEX_POINT('',#6390);
#2323=EDGE_CURVE('',#1912,#1912,#1652,.T.);
#2324=EDGE_CURVE('',#1912,#1913,#393,.T.);
#2325=EDGE_CURVE('',#1913,#1913,#1653,.T.);
#2326=EDGE_CURVE('',#1914,#1914,#1654,.T.);
#2327=EDGE_CURVE('',#1914,#1915,#394,.T.);
#2328=EDGE_CURVE('',#1915,#1915,#1655,.T.);
#2329=EDGE_CURVE('',#1916,#1916,#1656,.T.);
#2330=EDGE_CURVE('',#1916,#1917,#395,.T.);
#2331=EDGE_CURVE('',#1918,#1917,#1657,.T.);
#2332=EDGE_CURVE('',#1919,#1918,#1658,.T.);
#2333=EDGE_CURVE('',#1920,#1919,#1659,.T.);
#2334=EDGE_CURVE('',#1921,#1920,#1660,.T.);
#2335=EDGE_CURVE('',#1921,#1922,#1661,.T.);
#2336=EDGE_CURVE('',#1923,#1922,#1662,.T.);
#2337=EDGE_CURVE('',#1917,#1923,#1663,.T.);
#2338=EDGE_CURVE('',#1924,#1924,#1664,.T.);
#2339=EDGE_CURVE('',#1924,#1925,#396,.T.);
#2340=EDGE_CURVE('',#1925,#1925,#1665,.T.);
#2341=EDGE_CURVE('',#1926,#1927,#397,.T.);
#2342=EDGE_CURVE('',#1928,#1926,#398,.T.);
#2343=EDGE_CURVE('',#1929,#1928,#399,.T.);
#2344=EDGE_CURVE('',#1930,#1929,#400,.T.);
#2345=EDGE_CURVE('',#1931,#1930,#401,.T.);
#2346=EDGE_CURVE('',#1927,#1931,#402,.T.);
#2347=EDGE_CURVE('',#1932,#1926,#403,.T.);
#2348=EDGE_CURVE('',#1933,#1932,#404,.T.);
#2349=EDGE_CURVE('',#1933,#1928,#405,.T.);
#2350=EDGE_CURVE('',#1934,#1933,#406,.T.);
#2351=EDGE_CURVE('',#1934,#1929,#407,.T.);
#2352=EDGE_CURVE('',#1935,#1934,#408,.T.);
#2353=EDGE_CURVE('',#1935,#1930,#409,.T.);
#2354=EDGE_CURVE('',#1936,#1935,#410,.T.);
#2355=EDGE_CURVE('',#1936,#1931,#411,.T.);
#2356=EDGE_CURVE('',#1937,#1936,#412,.T.);
#2357=EDGE_CURVE('',#1937,#1927,#413,.T.);
#2358=EDGE_CURVE('',#1932,#1937,#414,.T.);
#2359=EDGE_CURVE('',#1938,#1939,#415,.T.);
#2360=EDGE_CURVE('',#1939,#1940,#416,.T.);
#2361=EDGE_CURVE('',#1940,#1941,#417,.T.);
#2362=EDGE_CURVE('',#1941,#1942,#418,.T.);
#2363=EDGE_CURVE('',#1942,#1943,#419,.T.);
#2364=EDGE_CURVE('',#1943,#1938,#420,.T.);
#2365=EDGE_CURVE('',#1923,#1944,#421,.T.);
#2366=EDGE_CURVE('',#1944,#1922,#422,.T.);
#2367=EDGE_CURVE('',#1922,#1945,#423,.T.);
#2368=EDGE_CURVE('',#1945,#1921,#424,.T.);
#2369=EDGE_CURVE('',#1921,#1946,#425,.T.);
#2370=EDGE_CURVE('',#1946,#1920,#426,.T.);
#2371=EDGE_CURVE('',#1920,#1947,#427,.T.);
#2372=EDGE_CURVE('',#1947,#1919,#428,.T.);
#2373=EDGE_CURVE('',#1919,#1948,#429,.T.);
#2374=EDGE_CURVE('',#1948,#1918,#430,.T.);
#2375=EDGE_CURVE('',#1918,#1949,#431,.T.);
#2376=EDGE_CURVE('',#1949,#1923,#432,.T.);
#2377=EDGE_CURVE('',#1939,#1948,#433,.T.);
#2378=EDGE_CURVE('',#1938,#1947,#434,.T.);
#2379=EDGE_CURVE('',#1940,#1949,#435,.T.);
#2380=EDGE_CURVE('',#1941,#1944,#436,.T.);
#2381=EDGE_CURVE('',#1942,#1945,#437,.T.);
#2382=EDGE_CURVE('',#1943,#1946,#438,.T.);
#3032=ORIENTED_EDGE('',*,*,#2323,.T.);
#3033=ORIENTED_EDGE('',*,*,#2324,.T.);
#3034=ORIENTED_EDGE('',*,*,#2325,.T.);
#3035=ORIENTED_EDGE('',*,*,#2324,.F.);
#3036=ORIENTED_EDGE('',*,*,#2326,.F.);
#3037=ORIENTED_EDGE('',*,*,#2327,.T.);
#3038=ORIENTED_EDGE('',*,*,#2328,.T.);
#3039=ORIENTED_EDGE('',*,*,#2327,.F.);
#3040=ORIENTED_EDGE('',*,*,#2329,.F.);
#3041=ORIENTED_EDGE('',*,*,#2330,.T.);
#3042=ORIENTED_EDGE('',*,*,#2331,.F.);
#3043=ORIENTED_EDGE('',*,*,#2332,.F.);
#3044=ORIENTED_EDGE('',*,*,#2333,.F.);
#3045=ORIENTED_EDGE('',*,*,#2334,.F.);
#3046=ORIENTED_EDGE('',*,*,#2335,.T.);
#3047=ORIENTED_EDGE('',*,*,#2336,.F.);
#3048=ORIENTED_EDGE('',*,*,#2337,.F.);
#3049=ORIENTED_EDGE('',*,*,#2330,.F.);
#3050=ORIENTED_EDGE('',*,*,#2338,.F.);
#3051=ORIENTED_EDGE('',*,*,#2339,.T.);
#3052=ORIENTED_EDGE('',*,*,#2340,.T.);
#3053=ORIENTED_EDGE('',*,*,#2339,.F.);
#3054=ORIENTED_EDGE('',*,*,#2338,.T.);
#3055=ORIENTED_EDGE('',*,*,#2341,.F.);
#3056=ORIENTED_EDGE('',*,*,#2342,.F.);
#3057=ORIENTED_EDGE('',*,*,#2343,.F.);
#3058=ORIENTED_EDGE('',*,*,#2344,.F.);
#3059=ORIENTED_EDGE('',*,*,#2345,.F.);
#3060=ORIENTED_EDGE('',*,*,#2346,.F.);
#3061=ORIENTED_EDGE('',*,*,#2340,.F.);
#3062=ORIENTED_EDGE('',*,*,#2329,.T.);
#3063=ORIENTED_EDGE('',*,*,#2342,.T.);
#3064=ORIENTED_EDGE('',*,*,#2347,.F.);
#3065=ORIENTED_EDGE('',*,*,#2348,.F.);
#3066=ORIENTED_EDGE('',*,*,#2349,.T.);
#3067=ORIENTED_EDGE('',*,*,#2343,.T.);
#3068=ORIENTED_EDGE('',*,*,#2349,.F.);
#3069=ORIENTED_EDGE('',*,*,#2350,.F.);
#3070=ORIENTED_EDGE('',*,*,#2351,.T.);
#3071=ORIENTED_EDGE('',*,*,#2344,.T.);
#3072=ORIENTED_EDGE('',*,*,#2351,.F.);
#3073=ORIENTED_EDGE('',*,*,#2352,.F.);
#3074=ORIENTED_EDGE('',*,*,#2353,.T.);
#3075=ORIENTED_EDGE('',*,*,#2345,.T.);
#3076=ORIENTED_EDGE('',*,*,#2353,.F.);
#3077=ORIENTED_EDGE('',*,*,#2354,.F.);
#3078=ORIENTED_EDGE('',*,*,#2355,.T.);
#3079=ORIENTED_EDGE('',*,*,#2346,.T.);
#3080=ORIENTED_EDGE('',*,*,#2355,.F.);
#3081=ORIENTED_EDGE('',*,*,#2356,.F.);
#3082=ORIENTED_EDGE('',*,*,#2357,.T.);
#3083=ORIENTED_EDGE('',*,*,#2341,.T.);
#3084=ORIENTED_EDGE('',*,*,#2357,.F.);
#3085=ORIENTED_EDGE('',*,*,#2358,.F.);
#3086=ORIENTED_EDGE('',*,*,#2347,.T.);
#3087=ORIENTED_EDGE('',*,*,#2348,.T.);
#3088=ORIENTED_EDGE('',*,*,#2358,.T.);
#3089=ORIENTED_EDGE('',*,*,#2356,.T.);
#3090=ORIENTED_EDGE('',*,*,#2354,.T.);
#3091=ORIENTED_EDGE('',*,*,#2352,.T.);
#3092=ORIENTED_EDGE('',*,*,#2350,.T.);
#3093=ORIENTED_EDGE('',*,*,#2359,.T.);
#3094=ORIENTED_EDGE('',*,*,#2360,.T.);
#3095=ORIENTED_EDGE('',*,*,#2361,.T.);
#3096=ORIENTED_EDGE('',*,*,#2362,.T.);
#3097=ORIENTED_EDGE('',*,*,#2363,.T.);
#3098=ORIENTED_EDGE('',*,*,#2364,.T.);
#3099=ORIENTED_EDGE('',*,*,#2323,.F.);
#3100=ORIENTED_EDGE('',*,*,#2365,.F.);
#3101=ORIENTED_EDGE('',*,*,#2336,.T.);
#3102=ORIENTED_EDGE('',*,*,#2366,.F.);
#3103=ORIENTED_EDGE('',*,*,#2367,.F.);
#3104=ORIENTED_EDGE('',*,*,#2335,.F.);
#3105=ORIENTED_EDGE('',*,*,#2368,.F.);
#3106=ORIENTED_EDGE('',*,*,#2369,.F.);
#3107=ORIENTED_EDGE('',*,*,#2334,.T.);
#3108=ORIENTED_EDGE('',*,*,#2370,.F.);
#3109=ORIENTED_EDGE('',*,*,#2371,.F.);
#3110=ORIENTED_EDGE('',*,*,#2333,.T.);
#3111=ORIENTED_EDGE('',*,*,#2372,.F.);
#3112=ORIENTED_EDGE('',*,*,#2373,.F.);
#3113=ORIENTED_EDGE('',*,*,#2332,.T.);
#3114=ORIENTED_EDGE('',*,*,#2374,.F.);
#3115=ORIENTED_EDGE('',*,*,#2375,.F.);
#3116=ORIENTED_EDGE('',*,*,#2331,.T.);
#3117=ORIENTED_EDGE('',*,*,#2337,.T.);
#3118=ORIENTED_EDGE('',*,*,#2376,.F.);
#3119=ORIENTED_EDGE('',*,*,#2372,.T.);
#3120=ORIENTED_EDGE('',*,*,#2373,.T.);
#3121=ORIENTED_EDGE('',*,*,#2377,.F.);
#3122=ORIENTED_EDGE('',*,*,#2359,.F.);
#3123=ORIENTED_EDGE('',*,*,#2378,.T.);
#3124=ORIENTED_EDGE('',*,*,#2374,.T.);
#3125=ORIENTED_EDGE('',*,*,#2375,.T.);
#3126=ORIENTED_EDGE('',*,*,#2379,.F.);
#3127=ORIENTED_EDGE('',*,*,#2360,.F.);
#3128=ORIENTED_EDGE('',*,*,#2377,.T.);
#3129=ORIENTED_EDGE('',*,*,#2376,.T.);
#3130=ORIENTED_EDGE('',*,*,#2365,.T.);
#3131=ORIENTED_EDGE('',*,*,#2380,.F.);
#3132=ORIENTED_EDGE('',*,*,#2361,.F.);
#3133=ORIENTED_EDGE('',*,*,#2379,.T.);
#3134=ORIENTED_EDGE('',*,*,#2366,.T.);
#3135=ORIENTED_EDGE('',*,*,#2367,.T.);
#3136=ORIENTED_EDGE('',*,*,#2381,.F.);
#3137=ORIENTED_EDGE('',*,*,#2362,.F.);
#3138=ORIENTED_EDGE('',*,*,#2380,.T.);
#3139=ORIENTED_EDGE('',*,*,#2368,.T.);
#3140=ORIENTED_EDGE('',*,*,#2369,.T.);
#3141=ORIENTED_EDGE('',*,*,#2382,.F.);
#3142=ORIENTED_EDGE('',*,*,#2363,.F.);
#3143=ORIENTED_EDGE('',*,*,#2381,.T.);
#3144=ORIENTED_EDGE('',*,*,#2370,.T.);
#3145=ORIENTED_EDGE('',*,*,#2371,.T.);
#3146=ORIENTED_EDGE('',*,*,#2378,.F.);
#3147=ORIENTED_EDGE('',*,*,#2364,.F.);
#3148=ORIENTED_EDGE('',*,*,#2382,.T.);
#3149=ORIENTED_EDGE('',*,*,#2328,.F.);
#3150=ORIENTED_EDGE('',*,*,#2325,.F.);
#3151=ORIENTED_EDGE('',*,*,#2326,.T.);
#3973=ADVANCED_FACE('',(#1138),#1020,.T.);
#3974=ADVANCED_FACE('',(#1139),#1021,.T.);
#3975=ADVANCED_FACE('',(#1140),#1022,.T.);
#3976=ADVANCED_FACE('',(#1141),#1023,.T.);
#3977=ADVANCED_FACE('',(#1142,#119),#194,.F.);
#3978=ADVANCED_FACE('',(#1143,#120),#195,.F.);
#3979=ADVANCED_FACE('',(#1144),#196,.F.);
#3980=ADVANCED_FACE('',(#1145),#197,.F.);
#3981=ADVANCED_FACE('',(#1146),#198,.F.);
#3982=ADVANCED_FACE('',(#1147),#199,.F.);
#3983=ADVANCED_FACE('',(#1148),#200,.F.);
#3984=ADVANCED_FACE('',(#1149),#201,.F.);
#3985=ADVANCED_FACE('',(#1150),#202,.F.);
#3986=ADVANCED_FACE('',(#1151,#121),#203,.T.);
#3987=ADVANCED_FACE('',(#1152),#204,.F.);
#3988=ADVANCED_FACE('',(#1153),#205,.F.);
#3989=ADVANCED_FACE('',(#1154),#206,.F.);
#3990=ADVANCED_FACE('',(#1155),#207,.F.);
#3991=ADVANCED_FACE('',(#1156),#208,.F.);
#3992=ADVANCED_FACE('',(#1157),#209,.F.);
#3993=ADVANCED_FACE('',(#1158),#210,.F.);
#3994=ADVANCED_FACE('',(#1159),#211,.F.);
#3995=ADVANCED_FACE('',(#1160),#212,.F.);
#3996=ADVANCED_FACE('',(#1161),#213,.F.);
#3997=ADVANCED_FACE('',(#1162),#214,.F.);
#3998=ADVANCED_FACE('',(#1163),#215,.F.);
#3999=ADVANCED_FACE('',(#1164),#216,.F.);
#4000=ADVANCED_FACE('',(#1165,#122),#217,.F.);
#4165=CLOSED_SHELL('',(#3973,#3974,#3975,#3976,#3977,#3978,#3979,#3980,
#3981,#3982,#3983,#3984,#3985,#3986,#3987,#3988,#3989,#3990,#3991,#3992,
#3993,#3994,#3995,#3996,#3997,#3998,#3999,#4000));
#4338=AXIS2_PLACEMENT_3D('',#6280,#4994,#4995);
#4339=AXIS2_PLACEMENT_3D('',#6281,#4996,#4997);
#4340=AXIS2_PLACEMENT_3D('',#6283,#4998,#4999);
#4341=AXIS2_PLACEMENT_3D('',#6286,#5001,#5002);
#4342=AXIS2_PLACEMENT_3D('',#6287,#5003,#5004);
#4343=AXIS2_PLACEMENT_3D('',#6289,#5005,#5006);
#4344=AXIS2_PLACEMENT_3D('',#6292,#5008,#5009);
#4345=AXIS2_PLACEMENT_3D('',#6293,#5010,#5011);
#4346=AXIS2_PLACEMENT_3D('',#6295,#5012,#5013);
#4347=AXIS2_PLACEMENT_3D('',#6299,#5015,#5016);
#4348=AXIS2_PLACEMENT_3D('',#6301,#5017,#5018);
#4349=AXIS2_PLACEMENT_3D('',#6303,#5019,#5020);
#4350=AXIS2_PLACEMENT_3D('',#6305,#5021,#5022);
#4351=AXIS2_PLACEMENT_3D('',#6307,#5023,#5024);
#4352=AXIS2_PLACEMENT_3D('',#6309,#5025,#5026);
#4353=AXIS2_PLACEMENT_3D('',#6310,#5027,#5028);
#4354=AXIS2_PLACEMENT_3D('',#6311,#5029,#5030);
#4355=AXIS2_PLACEMENT_3D('',#6313,#5031,#5032);
#4356=AXIS2_PLACEMENT_3D('',#6316,#5034,#5035);
#4357=AXIS2_PLACEMENT_3D('',#6317,#5036,#5037);
#4358=AXIS2_PLACEMENT_3D('',#6330,#5044,#5045);
#4359=AXIS2_PLACEMENT_3D('',#6331,#5046,#5047);
#4360=AXIS2_PLACEMENT_3D('',#6337,#5051,#5052);
#4361=AXIS2_PLACEMENT_3D('',#6341,#5055,#5056);
#4362=AXIS2_PLACEMENT_3D('',#6345,#5059,#5060);
#4363=AXIS2_PLACEMENT_3D('',#6349,#5063,#5064);
#4364=AXIS2_PLACEMENT_3D('',#6353,#5067,#5068);
#4365=AXIS2_PLACEMENT_3D('',#6355,#5070,#5071);
#4366=AXIS2_PLACEMENT_3D('',#6356,#5072,#5073);
#4367=AXIS2_PLACEMENT_3D('',#6369,#5080,#5081);
#4368=AXIS2_PLACEMENT_3D('',#6373,#5084,#5085);
#4369=AXIS2_PLACEMENT_3D('',#6377,#5088,#5089);
#4370=AXIS2_PLACEMENT_3D('',#6381,#5092,#5093);
#4371=AXIS2_PLACEMENT_3D('',#6385,#5096,#5097);
#4372=AXIS2_PLACEMENT_3D('',#6389,#5100,#5101);
#4373=AXIS2_PLACEMENT_3D('',#6393,#5104,#5105);
#4374=AXIS2_PLACEMENT_3D('',#6396,#5108,#5109);
#4375=AXIS2_PLACEMENT_3D('',#6398,#5111,#5112);
#4376=AXIS2_PLACEMENT_3D('',#6400,#5114,#5115);
#4377=AXIS2_PLACEMENT_3D('',#6402,#5117,#5118);
#4378=AXIS2_PLACEMENT_3D('',#6404,#5120,#5121);
#4379=AXIS2_PLACEMENT_3D('',#6405,#5122,#5123);
#4380=AXIS2_PLACEMENT_3D('',#6406,#5124,#5125);
#4994=DIRECTION('axis',(0.,0.,1.));
#4995=DIRECTION('refdir',(1.,0.,0.));
#4996=DIRECTION('center_axis',(0.,0.,1.));
#4997=DIRECTION('ref_axis',(1.,0.,0.));
#4998=DIRECTION('center_axis',(0.,0.,-1.));
#4999=DIRECTION('ref_axis',(-1.,0.,0.));
#5000=DIRECTION('',(0.,0.,-1.));
#5001=DIRECTION('center_axis',(0.,0.,1.));
#5002=DIRECTION('ref_axis',(1.,0.,0.));
#5003=DIRECTION('center_axis',(0.,0.,1.));
#5004=DIRECTION('ref_axis',(1.,0.,0.));
#5005=DIRECTION('center_axis',(0.,0.,1.));
#5006=DIRECTION('ref_axis',(1.,0.,0.));
#5007=DIRECTION('',(0.,0.,-1.));
#5008=DIRECTION('center_axis',(0.,0.,1.));
#5009=DIRECTION('ref_axis',(1.,0.,0.));
#5010=DIRECTION('center_axis',(0.,0.,1.));
#5011=DIRECTION('ref_axis',(1.,0.,0.));
#5012=DIRECTION('center_axis',(0.,0.,1.));
#5013=DIRECTION('ref_axis',(1.,0.,0.));
#5014=DIRECTION('',(0.,0.,-1.));
#5015=DIRECTION('center_axis',(0.,0.,-1.));
#5016=DIRECTION('ref_axis',(-1.,0.,0.));
#5017=DIRECTION('center_axis',(0.,0.,-1.));
#5018=DIRECTION('ref_axis',(-1.,0.,0.));
#5019=DIRECTION('center_axis',(0.,0.,-1.));
#5020=DIRECTION('ref_axis',(-1.,0.,0.));
#5021=DIRECTION('center_axis',(0.,0.,-1.));
#5022=DIRECTION('ref_axis',(-1.,0.,0.));
#5023=DIRECTION('center_axis',(0.,0.,1.));
#5024=DIRECTION('ref_axis',(1.,0.,0.));
#5025=DIRECTION('center_axis',(0.,0.,-1.));
#5026=DIRECTION('ref_axis',(-1.,0.,0.));
#5027=DIRECTION('center_axis',(0.,0.,-1.));
#5028=DIRECTION('ref_axis',(-1.,0.,0.));
#5029=DIRECTION('center_axis',(0.,0.,1.));
#5030=DIRECTION('ref_axis',(1.,0.,0.));
#5031=DIRECTION('center_axis',(0.,0.,1.));
#5032=DIRECTION('ref_axis',(1.,0.,0.));
#5033=DIRECTION('',(0.,0.,-1.));
#5034=DIRECTION('center_axis',(0.,0.,1.));
#5035=DIRECTION('ref_axis',(1.,0.,0.));
#5036=DIRECTION('center_axis',(0.,0.,-1.));
#5037=DIRECTION('ref_axis',(-1.,0.,0.));
#5038=DIRECTION('',(-0.5,0.866025403784438,0.));
#5039=DIRECTION('',(0.5,0.866025403784439,0.));
#5040=DIRECTION('',(1.,-1.25192883228096E-16,0.));
#5041=DIRECTION('',(0.5,-0.866025403784439,0.));
#5042=DIRECTION('',(-0.5,-0.866025403784439,0.));
#5043=DIRECTION('',(-1.,0.,0.));
#5044=DIRECTION('center_axis',(0.,0.,1.));
#5045=DIRECTION('ref_axis',(1.,0.,0.));
#5046=DIRECTION('center_axis',(0.866025403784439,-0.5,0.));
#5047=DIRECTION('ref_axis',(0.5,0.866025403784439,0.));
#5048=DIRECTION('',(0.,0.,1.));
#5049=DIRECTION('',(0.5,0.866025403784439,0.));
#5050=DIRECTION('',(0.,0.,1.));
#5051=DIRECTION('center_axis',(-1.25192883228096E-16,-1.,0.));
#5052=DIRECTION('ref_axis',(1.,-1.25192883228096E-16,0.));
#5053=DIRECTION('',(1.,-1.25192883228096E-16,0.));
#5054=DIRECTION('',(0.,0.,1.));
#5055=DIRECTION('center_axis',(-0.866025403784439,-0.5,0.));
#5056=DIRECTION('ref_axis',(0.5,-0.866025403784439,0.));
#5057=DIRECTION('',(0.5,-0.866025403784439,0.));
#5058=DIRECTION('',(0.,0.,1.));
#5059=DIRECTION('center_axis',(-0.866025403784439,0.5,0.));
#5060=DIRECTION('ref_axis',(-0.5,-0.866025403784439,0.));
#5061=DIRECTION('',(-0.5,-0.866025403784439,0.));
#5062=DIRECTION('',(0.,0.,1.));
#5063=DIRECTION('center_axis',(0.,1.,0.));
#5064=DIRECTION('ref_axis',(0.,0.,1.));
#5065=DIRECTION('',(-1.,0.,0.));
#5066=DIRECTION('',(0.,0.,1.));
#5067=DIRECTION('center_axis',(0.866025403784439,0.5,0.));
#5068=DIRECTION('ref_axis',(-0.5,0.866025403784439,0.));
#5069=DIRECTION('',(-0.5,0.866025403784438,0.));
#5070=DIRECTION('center_axis',(0.,0.,-1.));
#5071=DIRECTION('ref_axis',(-1.,0.,0.));
#5072=DIRECTION('center_axis',(0.,0.,-1.));
#5073=DIRECTION('ref_axis',(-1.,0.,0.));
#5074=DIRECTION('',(-0.995844981312748,-0.0910646649047396,0.));
#5075=DIRECTION('',(-0.576786803850996,0.816894719595709,0.));
#5076=DIRECTION('',(0.419058177461752,0.907959384500449,0.));
#5077=DIRECTION('',(0.995844981312748,0.0910646649047398,0.));
#5078=DIRECTION('',(0.576786803850996,-0.816894719595709,0.));
#5079=DIRECTION('',(-0.419058177461752,-0.907959384500449,0.));
#5080=DIRECTION('center_axis',(0.,0.,-1.));
#5081=DIRECTION('ref_axis',(-1.,0.,0.));
#5082=DIRECTION('',(0.419058177461752,0.907959384500449,0.));
#5083=DIRECTION('',(0.995844981312748,0.0910646649047398,0.));
#5084=DIRECTION('center_axis',(0.,0.,-1.));
#5085=DIRECTION('ref_axis',(-1.,0.,0.));
#5086=DIRECTION('',(0.995844981312748,0.0910646649047398,0.));
#5087=DIRECTION('',(0.576786803850996,-0.816894719595709,0.));
#5088=DIRECTION('center_axis',(0.,0.,-1.));
#5089=DIRECTION('ref_axis',(-1.,0.,0.));
#5090=DIRECTION('',(0.576786803850996,-0.816894719595709,0.));
#5091=DIRECTION('',(-0.419058177461752,-0.907959384500449,0.));
#5092=DIRECTION('center_axis',(0.,0.,-1.));
#5093=DIRECTION('ref_axis',(-1.,0.,0.));
#5094=DIRECTION('',(-0.419058177461752,-0.907959384500449,0.));
#5095=DIRECTION('',(-0.995844981312748,-0.0910646649047396,0.));
#5096=DIRECTION('center_axis',(0.,0.,-1.));
#5097=DIRECTION('ref_axis',(-1.,0.,0.));
#5098=DIRECTION('',(-0.995844981312748,-0.0910646649047396,0.));
#5099=DIRECTION('',(-0.576786803850996,0.816894719595709,0.));
#5100=DIRECTION('center_axis',(0.,0.,-1.));
#5101=DIRECTION('ref_axis',(-1.,0.,0.));
#5102=DIRECTION('',(-0.576786803850996,0.816894719595709,0.));
#5103=DIRECTION('',(0.419058177461752,0.907959384500449,0.));
#5104=DIRECTION('center_axis',(-0.0910646649047396,0.995844981312748,0.));
#5105=DIRECTION('ref_axis',(-0.995844981312748,-0.0910646649047396,0.));
#5106=DIRECTION('',(0.,0.,1.));
#5107=DIRECTION('',(0.,0.,1.));
#5108=DIRECTION('center_axis',(0.816894719595709,0.576786803850996,0.));
#5109=DIRECTION('ref_axis',(-0.576786803850996,0.816894719595709,0.));
#5110=DIRECTION('',(0.,0.,1.));
#5111=DIRECTION('center_axis',(0.907959384500449,-0.419058177461752,0.));
#5112=DIRECTION('ref_axis',(0.419058177461752,0.907959384500449,0.));
#5113=DIRECTION('',(0.,0.,1.));
#5114=DIRECTION('center_axis',(0.0910646649047398,-0.995844981312748,0.));
#5115=DIRECTION('ref_axis',(0.995844981312748,0.0910646649047399,0.));
#5116=DIRECTION('',(0.,0.,1.));
#5117=DIRECTION('center_axis',(-0.816894719595709,-0.576786803850996,0.));
#5118=DIRECTION('ref_axis',(0.576786803850996,-0.816894719595709,0.));
#5119=DIRECTION('',(0.,0.,1.));
#5120=DIRECTION('center_axis',(-0.907959384500449,0.419058177461752,0.));
#5121=DIRECTION('ref_axis',(-0.419058177461752,-0.907959384500449,0.));
#5122=DIRECTION('center_axis',(0.,0.,1.));
#5123=DIRECTION('ref_axis',(1.,0.,0.));
#5124=DIRECTION('center_axis',(0.,0.,1.));
#5125=DIRECTION('ref_axis',(1.,0.,0.));
#6280=CARTESIAN_POINT('',(0.,0.,0.));
#6281=CARTESIAN_POINT('Origin',(0.,0.,67.));
#6282=CARTESIAN_POINT('',(-6.,-7.34788079488412E-16,-68.));
#6283=CARTESIAN_POINT('Origin',(0.,0.,-68.));
#6284=CARTESIAN_POINT('',(-6.,-7.34788079488412E-16,-148.));
#6285=CARTESIAN_POINT('',(-6.,-7.34788079488412E-16,67.));
#6286=CARTESIAN_POINT('Origin',(0.,0.,-148.));
#6287=CARTESIAN_POINT('Origin',(0.,0.,67.));
#6288=CARTESIAN_POINT('',(-5.,-6.12323399573677E-16,-148.));
#6289=CARTESIAN_POINT('Origin',(0.,0.,-148.));
#6290=CARTESIAN_POINT('',(-5.,-6.12323399573677E-16,-170.));
#6291=CARTESIAN_POINT('',(-5.,-6.12323399573677E-16,67.));
#6292=CARTESIAN_POINT('Origin',(0.,0.,-170.));
#6293=CARTESIAN_POINT('Origin',(0.,0.,67.));
#6294=CARTESIAN_POINT('',(-10.,-1.22464679914735E-15,-14.));
#6295=CARTESIAN_POINT('Origin',(0.,0.,-14.));
#6296=CARTESIAN_POINT('',(-10.,-1.22464679914735E-15,-60.));
#6297=CARTESIAN_POINT('',(-10.,-1.22464679914735E-15,67.));
#6298=CARTESIAN_POINT('',(-8.1689471959571,-5.76786803850996,-60.));
#6299=CARTESIAN_POINT('Origin',(0.,0.,-60.));
#6300=CARTESIAN_POINT('',(0.910646649047397,-9.95844981312749,-60.));
#6301=CARTESIAN_POINT('Origin',(0.,0.,-60.));
#6302=CARTESIAN_POINT('',(9.07959384500449,-4.19058177461752,-60.));
#6303=CARTESIAN_POINT('Origin',(0.,0.,-60.));
#6304=CARTESIAN_POINT('',(8.1689471959571,5.76786803850996,-60.));
#6305=CARTESIAN_POINT('Origin',(0.,0.,-60.));
#6306=CARTESIAN_POINT('',(-0.910646649047399,9.95844981312748,-60.));
#6307=CARTESIAN_POINT('Origin',(0.,0.,-60.));
#6308=CARTESIAN_POINT('',(-9.0795938450045,4.19058177461752,-60.));
#6309=CARTESIAN_POINT('Origin',(0.,0.,-60.));
#6310=CARTESIAN_POINT('Origin',(0.,0.,-60.));
#6311=CARTESIAN_POINT('Origin',(0.,0.,67.));
#6312=CARTESIAN_POINT('',(-14.,-1.71450551880629E-15,0.));
#6313=CARTESIAN_POINT('Origin',(0.,0.,0.));
#6314=CARTESIAN_POINT('',(-14.,-1.71450551880629E-15,-14.));
#6315=CARTESIAN_POINT('',(-14.,-1.71450551880629E-15,67.));
#6316=CARTESIAN_POINT('Origin',(0.,0.,-14.));
#6317=CARTESIAN_POINT('Origin',(0.,0.,0.));
#6318=CARTESIAN_POINT('',(6.92820323027551,1.73472347597681E-15,0.));
#6319=CARTESIAN_POINT('',(3.46410161513776,6.,0.));
#6320=CARTESIAN_POINT('',(6.92820323027551,1.73472347597681E-15,0.));
#6321=CARTESIAN_POINT('',(3.46410161513776,-6.,0.));
#6322=CARTESIAN_POINT('',(3.46410161513776,-6.,0.));
#6323=CARTESIAN_POINT('',(-3.46410161513776,-6.,0.));
#6324=CARTESIAN_POINT('',(-3.46410161513776,-6.,0.));
#6325=CARTESIAN_POINT('',(-6.92820323027551,6.71609035746146E-16,0.));
#6326=CARTESIAN_POINT('',(-6.92820323027551,6.71609035746146E-16,0.));
#6327=CARTESIAN_POINT('',(-3.46410161513776,6.,0.));
#6328=CARTESIAN_POINT('',(-3.46410161513776,6.,0.));
#6329=CARTESIAN_POINT('',(3.46410161513776,6.,0.));
#6330=CARTESIAN_POINT('Origin',(0.,14.,-14.));
#6331=CARTESIAN_POINT('Origin',(3.46410161513776,-6.,-10.));
#6332=CARTESIAN_POINT('',(6.92820323027551,1.73472347597681E-15,-10.));
#6333=CARTESIAN_POINT('',(6.92820323027551,1.73472347597681E-15,-10.));
#6334=CARTESIAN_POINT('',(3.46410161513776,-6.,-10.));
#6335=CARTESIAN_POINT('',(3.46410161513776,-6.,-10.));
#6336=CARTESIAN_POINT('',(3.46410161513776,-6.,-10.));
#6337=CARTESIAN_POINT('Origin',(-3.46410161513776,-6.,-10.));
#6338=CARTESIAN_POINT('',(-3.46410161513776,-6.,-10.));
#6339=CARTESIAN_POINT('',(-3.46410161513776,-6.,-10.));
#6340=CARTESIAN_POINT('',(-3.46410161513776,-6.,-10.));
#6341=CARTESIAN_POINT('Origin',(-6.92820323027551,6.71609035746146E-16,
-10.));
#6342=CARTESIAN_POINT('',(-6.92820323027551,6.71609035746146E-16,-10.));
#6343=CARTESIAN_POINT('',(-6.92820323027551,6.71609035746146E-16,-10.));
#6344=CARTESIAN_POINT('',(-6.92820323027551,6.71609035746146E-16,-10.));
#6345=CARTESIAN_POINT('Origin',(-3.46410161513776,6.,-10.));
#6346=CARTESIAN_POINT('',(-3.46410161513776,6.,-10.));
#6347=CARTESIAN_POINT('',(-3.46410161513776,6.,-10.));
#6348=CARTESIAN_POINT('',(-3.46410161513776,6.,-10.));
#6349=CARTESIAN_POINT('Origin',(3.46410161513776,6.,-10.));
#6350=CARTESIAN_POINT('',(3.46410161513776,6.,-10.));
#6351=CARTESIAN_POINT('',(3.46410161513776,6.,-10.));
#6352=CARTESIAN_POINT('',(3.46410161513776,6.,-10.));
#6353=CARTESIAN_POINT('Origin',(6.92820323027551,1.73472347597681E-15,-10.));
#6354=CARTESIAN_POINT('',(6.92820323027551,1.73472347597681E-15,-10.));
#6355=CARTESIAN_POINT('Origin',(3.46410161513776,-6.,-10.));
#6356=CARTESIAN_POINT('Origin',(-16.3378943919142,-11.5357360770199,-68.));
#6357=CARTESIAN_POINT('',(6.66016032936793,-9.43268772516334,-68.));
#6358=CARTESIAN_POINT('',(-4.83886703127313,-10.4842119010916,-68.));
#6359=CARTESIAN_POINT('',(6.66016032936793,-9.43268772516334,-68.));
#6360=CARTESIAN_POINT('',(-11.4990273606411,-1.0515241759283,-68.));
#6361=CARTESIAN_POINT('',(-4.83886703127313,-10.4842119010916,-68.));
#6362=CARTESIAN_POINT('',(-6.66016032936793,9.43268772516333,-68.));
#6363=CARTESIAN_POINT('',(-11.4990273606411,-1.0515241759283,-68.));
#6364=CARTESIAN_POINT('',(4.83886703127313,10.4842119010916,-68.));
#6365=CARTESIAN_POINT('',(-6.66016032936793,9.43268772516333,-68.));
#6366=CARTESIAN_POINT('',(11.4990273606411,1.05152417592829,-68.));
#6367=CARTESIAN_POINT('',(4.83886703127313,10.4842119010916,-68.));
#6368=CARTESIAN_POINT('',(11.4990273606411,1.05152417592829,-68.));
#6369=CARTESIAN_POINT('Origin',(-16.3378943919142,-11.5357360770199,-60.));
#6370=CARTESIAN_POINT('',(-6.66016032936793,9.43268772516333,-60.));
#6371=CARTESIAN_POINT('',(-11.4990273606411,-1.0515241759283,-60.));
#6372=CARTESIAN_POINT('',(-6.66016032936793,9.43268772516333,-60.));
#6373=CARTESIAN_POINT('Origin',(-16.3378943919142,-11.5357360770199,-60.));
#6374=CARTESIAN_POINT('',(4.83886703127313,10.4842119010916,-60.));
#6375=CARTESIAN_POINT('',(-6.66016032936793,9.43268772516333,-60.));
#6376=CARTESIAN_POINT('',(4.83886703127313,10.4842119010916,-60.));
#6377=CARTESIAN_POINT('Origin',(-16.3378943919142,-11.5357360770199,-60.));
#6378=CARTESIAN_POINT('',(11.4990273606411,1.05152417592829,-60.));
#6379=CARTESIAN_POINT('',(4.83886703127313,10.4842119010916,-60.));
#6380=CARTESIAN_POINT('',(11.4990273606411,1.05152417592829,-60.));
#6381=CARTESIAN_POINT('Origin',(-16.3378943919142,-11.5357360770199,-60.));
#6382=CARTESIAN_POINT('',(6.66016032936793,-9.43268772516334,-60.));
#6383=CARTESIAN_POINT('',(11.4990273606411,1.05152417592829,-60.));
#6384=CARTESIAN_POINT('',(6.66016032936793,-9.43268772516334,-60.));
#6385=CARTESIAN_POINT('Origin',(-16.3378943919142,-11.5357360770199,-60.));
#6386=CARTESIAN_POINT('',(-4.83886703127313,-10.4842119010916,-60.));
#6387=CARTESIAN_POINT('',(6.66016032936793,-9.43268772516334,-60.));
#6388=CARTESIAN_POINT('',(-4.83886703127313,-10.4842119010916,-60.));
#6389=CARTESIAN_POINT('Origin',(-16.3378943919142,-11.5357360770199,-60.));
#6390=CARTESIAN_POINT('',(-11.4990273606411,-1.0515241759283,-60.));
#6391=CARTESIAN_POINT('',(-4.83886703127313,-10.4842119010916,-60.));
#6392=CARTESIAN_POINT('',(-11.4990273606411,-1.0515241759283,-60.));
#6393=CARTESIAN_POINT('Origin',(6.66016032936793,-9.43268772516334,-68.));
#6394=CARTESIAN_POINT('',(-4.83886703127313,-10.4842119010916,-68.));
#6395=CARTESIAN_POINT('',(6.66016032936793,-9.43268772516334,-68.));
#6396=CARTESIAN_POINT('Origin',(-4.83886703127313,-10.4842119010916,-68.));
#6397=CARTESIAN_POINT('',(-11.4990273606411,-1.0515241759283,-68.));
#6398=CARTESIAN_POINT('Origin',(-11.4990273606411,-1.0515241759283,-68.));
#6399=CARTESIAN_POINT('',(-6.66016032936793,9.43268772516333,-68.));
#6400=CARTESIAN_POINT('Origin',(-6.66016032936793,9.43268772516333,-68.));
#6401=CARTESIAN_POINT('',(4.83886703127313,10.4842119010916,-68.));
#6402=CARTESIAN_POINT('Origin',(4.83886703127313,10.4842119010916,-68.));
#6403=CARTESIAN_POINT('',(11.4990273606411,1.05152417592829,-68.));
#6404=CARTESIAN_POINT('Origin',(11.4990273606411,1.05152417592829,-68.));
#6405=CARTESIAN_POINT('Origin',(0.,5.,-170.));
#6406=CARTESIAN_POINT('Origin',(0.,6.,-148.));
#7767=UNCERTAINTY_MEASURE_WITH_UNIT(LENGTH_MEASURE(0.01),#7784,
'DISTANCE_ACCURACY_VALUE',
'Maximum model space distance between geometric entities at asserted c
onnectivities');
#7773=UNCERTAINTY_MEASURE_WITH_UNIT(LENGTH_MEASURE(0.01),#7784,
'DISTANCE_ACCURACY_VALUE',
'Maximum model space distance between geometric entities at asserted c
onnectivities');
#7777=(
GEOMETRIC_REPRESENTATION_CONTEXT(3)
GLOBAL_UNCERTAINTY_ASSIGNED_CONTEXT((#7767))
GLOBAL_UNIT_ASSIGNED_CONTEXT((#7784,#7786,#7787))
REPRESENTATION_CONTEXT('','3D')
);
#7783=(
GEOMETRIC_REPRESENTATION_CONTEXT(3)
GLOBAL_UNCERTAINTY_ASSIGNED_CONTEXT((#7773))
GLOBAL_UNIT_ASSIGNED_CONTEXT((#7784,#7786,#7787))
REPRESENTATION_CONTEXT('','3D')
);
#7784=(
LENGTH_UNIT()
NAMED_UNIT(*)
SI_UNIT(.MILLI.,.METRE.)
);
#7786=(
NAMED_UNIT(*)
PLANE_ANGLE_UNIT()
SI_UNIT($,.RADIAN.)
);
#7787=(
NAMED_UNIT(*)
SI_UNIT($,.STERADIAN.)
SOLID_ANGLE_UNIT()
);
#7791=SHAPE_DEFINITION_REPRESENTATION(#7801,#7821);
#7801=PRODUCT_DEFINITION_SHAPE('',$,#7831);
#7821=SHAPE_REPRESENTATION('',(#4338),#7777);
#7827=PRODUCT_DEFINITION_CONTEXT('part definition',#7856,'design');
#7831=PRODUCT_DEFINITION('Screw','Screw',#7840,#7827);
#7840=PRODUCT_DEFINITION_FORMATION('',$,#7861);
#7856=APPLICATION_CONTEXT(
'Core Data for Automotive Mechanical Design Process');
#7857=PRODUCT_CONTEXT('part definition',#7856,'mechanical');
#7861=PRODUCT('Screw','Screw',$,(#7857));
#7869=PRESENTATION_STYLE_ASSIGNMENT((#7874));
#7874=SURFACE_STYLE_USAGE(.BOTH.,#7879);
#7879=SURFACE_SIDE_STYLE('',(#7884));
#7884=SURFACE_STYLE_FILL_AREA(#7889);
#7889=FILL_AREA_STYLE('Opaque(31,36,43)',(#7894));
#7894=FILL_AREA_STYLE_COLOUR('Opaque(31,36,43)',#7899);
#7899=COLOUR_RGB('Opaque(31,36,43)',0.12156862745098,0.141176470588235,
0.168627450980392);
ENDSEC;
END-ISO-10303-21;
